ISO-10303-21;
HEADER;
/* Generated by software containing ST-Developer
 * from STEP Tools, Inc. (www.steptools.com) 
 */

FILE_DESCRIPTION(
/* description */ ('Lifting hook block with sheave'),
/* implementation_level */ '2;1');

FILE_NAME(
/* name */ 'Swivel thrust washer.step',
/* time_stamp */ '2026-10-28T03:23:54-07:00',
/* author */ (''),
/* organization */ (''),
/* preprocessor_version */ 'ST-DEVELOPER v20.2',
/* originating_system */ 'Autodesk Translation Framework v15.17.0.0',
/* authorisation */ '');

FILE_SCHEMA (('AUTOMOTIVE_DESIGN { 1 0 10303 214 3 1 1 }'));
ENDSEC;

DATA;
#10=MECHANICAL_DESIGN_GEOMETRIC_PRESENTATION_REPRESENTATION('',(#386),#9391);
#318=SHAPE_REPRESENTATION_RELATIONSHIP('SRR','None',#9552,#348);
#348=ADVANCED_BREP_SHAPE_REPRESENTATION('',(#421),#9387);
#386=STYLED_ITEM('',(#9766),#421);
#421=MANIFOLD_SOLID_BREP('Body1',#4925);
#687=LINE('',#9227,#975);
#688=LINE('',#9233,#976);
#975=VECTOR('',#7448,0.81);
#976=VECTOR('',#7455,1.5);
#1100=CYLINDRICAL_SURFACE('',#5885,0.81);
#1101=CYLINDRICAL_SURFACE('',#5888,1.5);
#1214=FACE_BOUND('',#1891,.T.);
#1215=FACE_BOUND('',#1893,.T.);
#1492=FACE_OUTER_BOUND('',#1888,.T.);
#1493=FACE_OUTER_BOUND('',#1889,.T.);
#1494=FACE_OUTER_BOUND('',#1890,.T.);
#1495=FACE_OUTER_BOUND('',#1892,.T.);
#1888=EDGE_LOOP('',(#4374,#4375,#4376,#4377));
#1889=EDGE_LOOP('',(#4378,#4379,#4380,#4381));
#1890=EDGE_LOOP('',(#4382));
#1891=EDGE_LOOP('',(#4383));
#1892=EDGE_LOOP('',(#4384));
#1893=EDGE_LOOP('',(#4385));
#2194=CIRCLE('',#5886,0.81);
#2195=CIRCLE('',#5887,0.81);
#2196=CIRCLE('',#5889,1.5);
#2197=CIRCLE('',#5890,1.5);
#2593=VERTEX_POINT('',#9224);
#2594=VERTEX_POINT('',#9226);
#2595=VERTEX_POINT('',#9230);
#2596=VERTEX_POINT('',#9232);
#3191=EDGE_CURVE('',#2593,#2593,#2194,.T.);
#3192=EDGE_CURVE('',#2593,#2594,#687,.T.);
#3193=EDGE_CURVE('',#2594,#2594,#2195,.T.);
#3194=EDGE_CURVE('',#2595,#2595,#2196,.T.);
#3195=EDGE_CURVE('',#2595,#2596,#688,.T.);
#3196=EDGE_CURVE('',#2596,#2596,#2197,.T.);
#4374=ORIENTED_EDGE('',*,*,#3191,.F.);
#4375=ORIENTED_EDGE('',*,*,#3192,.T.);
#4376=ORIENTED_EDGE('',*,*,#3193,.T.);
#4377=ORIENTED_EDGE('',*,*,#3192,.F.);
#4378=ORIENTED_EDGE('',*,*,#3194,.F.);
#4379=ORIENTED_EDGE('',*,*,#3195,.T.);
#4380=ORIENTED_EDGE('',*,*,#3196,.T.);
#4381=ORIENTED_EDGE('',*,*,#3195,.F.);
#4382=ORIENTED_EDGE('',*,*,#3194,.T.);
#4383=ORIENTED_EDGE('',*,*,#3191,.T.);
#4384=ORIENTED_EDGE('',*,*,#3196,.F.);
#4385=ORIENTED_EDGE('',*,*,#3193,.F.);
#4586=PLANE('',#5891);
#4587=PLANE('',#5892);
#4868=ADVANCED_FACE('',(#1492),#1100,.F.);
#4869=ADVANCED_FACE('',(#1493),#1101,.T.);
#4870=ADVANCED_FACE('',(#1494,#1214),#4586,.T.);
#4871=ADVANCED_FACE('',(#1495,#1215),#4587,.F.);
#4925=CLOSED_SHELL('',(#4868,#4869,#4870,#4871));
#5884=AXIS2_PLACEMENT_3D('',#9222,#7442,#7443);
#5885=AXIS2_PLACEMENT_3D('',#9223,#7444,#7445);
#5886=AXIS2_PLACEMENT_3D('',#9225,#7446,#7447);
#5887=AXIS2_PLACEMENT_3D('',#9228,#7449,#7450);
#5888=AXIS2_PLACEMENT_3D('',#9229,#7451,#7452);
#5889=AXIS2_PLACEMENT_3D('',#9231,#7453,#7454);
#5890=AXIS2_PLACEMENT_3D('',#9234,#7456,#7457);
#5891=AXIS2_PLACEMENT_3D('',#9235,#7458,#7459);
#5892=AXIS2_PLACEMENT_3D('',#9236,#7460,#7461);
#7442=DIRECTION('axis',(0.,0.,1.));
#7443=DIRECTION('refdir',(1.,0.,0.));
#7444=DIRECTION('center_axis',(0.,0.,1.));
#7445=DIRECTION('ref_axis',(1.,0.,0.));
#7446=DIRECTION('center_axis',(0.,0.,-1.));
#7447=DIRECTION('ref_axis',(1.,0.,0.));
#7448=DIRECTION('',(0.,0.,-1.));
#7449=DIRECTION('center_axis',(0.,0.,-1.));
#7450=DIRECTION('ref_axis',(1.,0.,0.));
#7451=DIRECTION('center_axis',(0.,0.,1.));
#7452=DIRECTION('ref_axis',(1.,0.,0.));
#7453=DIRECTION('center_axis',(0.,0.,1.));
#7454=DIRECTION('ref_axis',(1.,0.,0.));
#7455=DIRECTION('',(0.,0.,-1.));
#7456=DIRECTION('center_axis',(0.,0.,1.));
#7457=DIRECTION('ref_axis',(1.,0.,0.));
#7458=DIRECTION('center_axis',(0.,0.,1.));
#7459=DIRECTION('ref_axis',(1.,0.,0.));
#7460=DIRECTION('center_axis',(0.,0.,1.));
#7461=DIRECTION('ref_axis',(1.,0.,0.));
#9222=CARTESIAN_POINT('',(0.,0.,0.));
#9223=CARTESIAN_POINT('Origin',(0.,0.,5.5));
#9224=CARTESIAN_POINT('',(-0.81,-9.91963907309356E-17,5.7));
#9225=CARTESIAN_POINT('Origin',(0.,0.,5.7));
#9226=CARTESIAN_POINT('',(-0.81,-9.91963907309356E-17,5.5));
#9227=CARTESIAN_POINT('',(-0.81,-9.91963907309356E-17,5.5));
#9228=CARTESIAN_POINT('Origin',(0.,0.,5.5));
#9229=CARTESIAN_POINT('Origin',(0.,0.,5.5));
#9230=CARTESIAN_POINT('',(-1.5,-1.83697019872103E-16,5.7));
#9231=CARTESIAN_POINT('Origin',(0.,0.,5.7));
#9232=CARTESIAN_POINT('',(-1.5,-1.83697019872103E-16,5.5));
#9233=CARTESIAN_POINT('',(-1.5,-1.83697019872103E-16,5.5));
#9234=CARTESIAN_POINT('Origin',(0.,0.,5.5));
#9235=CARTESIAN_POINT('Origin',(0.,0.,5.7));
#9236=CARTESIAN_POINT('Origin',(0.,0.,5.5));
#9350=UNCERTAINTY_MEASURE_WITH_UNIT(LENGTH_MEASURE(0.001),#9392,
'DISTANCE_ACCURACY_VALUE',
'Maximum model space distance between geometric entities at asserted c
onnectivities');
#9354=UNCERTAINTY_MEASURE_WITH_UNIT(LENGTH_MEASURE(0.001),#9392,
'DISTANCE_ACCURACY_VALUE',
'Maximum model space distance between geometric entities at asserted c
onnectivities');
#9387=(
GEOMETRIC_REPRESENTATION_CONTEXT(3)
GLOBAL_UNCERTAINTY_ASSIGNED_CONTEXT((#9350))
GLOBAL_UNIT_ASSIGNED_CONTEXT((#9392,#9394,#9395))
REPRESENTATION_CONTEXT('','3D')
);
#9391=(
GEOMETRIC_REPRESENTATION_CONTEXT(3)
GLOBAL_UNCERTAINTY_ASSIGNED_CONTEXT((#9354))
GLOBAL_UNIT_ASSIGNED_CONTEXT((#9392,#9394,#9395))
REPRESENTATION_CONTEXT('','3D')
);
#9392=(
LENGTH_UNIT()
NAMED_UNIT(*)
SI_UNIT(.CENTI.,.METRE.)
);
#9394=(
NAMED_UNIT(*)
PLANE_ANGLE_UNIT()
SI_UNIT($,.RADIAN.)
);
#9395=(
NAMED_UNIT(*)
SI_UNIT($,.STERADIAN.)
SOLID_ANGLE_UNIT()
);
#9428=SHAPE_DEFINITION_REPRESENTATION(#9508,#9552);
#9508=PRODUCT_DEFINITION_SHAPE('',$,#9589);
#9552=SHAPE_REPRESENTATION('',(#5884),#9387);
#9556=PRODUCT_DEFINITION_CONTEXT('part definition',#9666,'design');
#9589=PRODUCT_DEFINITION('Swivel thrust washer','Swivel thrust washer',
#9625,#9556);
#9625=PRODUCT_DEFINITION_FORMATION('',$,#9700);
#9666=APPLICATION_CONTEXT(
'Core Data for Automotive Mechanical Design Process');
#9667=PRODUCT_CONTEXT('part definition',#9666,'mechanical');
#9700=PRODUCT('Swivel thrust washer','Swivel thrust washer',
'Swivel thrust washer',(#9667));
#9760=COLOUR_RGB('Black',0.12,0.14,0.17);
#9761=FILL_AREA_STYLE_COLOUR('',#9760);
#9762=FILL_AREA_STYLE('',(#9761));
#9763=SURFACE_STYLE_FILL_AREA(#9762);
#9764=SURFACE_SIDE_STYLE('',(#9763));
#9765=SURFACE_STYLE_USAGE(.BOTH.,#9764);
#9766=PRESENTATION_STYLE_ASSIGNMENT((#9765));
ENDSEC;
END-ISO-10303-21;
